ISO-10303-21;
HEADER;
/* Generated by software containing ST-Developer
 * from STEP Tools, Inc. (www.steptools.com) 
 */

FILE_DESCRIPTION(
/* description */ ('PAT-065'),
/* implementation_level */ '2;1');

FILE_NAME(
/* name */ 'Rubber base.step',
/* time_stamp */ '2026-10-28T22:09:22-07:00',
/* author */ (''),
/* organization */ (''),
/* preprocessor_version */ 'ST-DEVELOPER v20.2',
/* originating_system */ 'Autodesk Translation Framework v15.17.0.0',
/* authorisation */ '');

FILE_SCHEMA (('AUTOMOTIVE_DESIGN { 1 0 10303 214 3 1 1 }'));
ENDSEC;

DATA;
#10=MECHANICAL_DESIGN_GEOMETRIC_PRESENTATION_REPRESENTATION('',(#162),#5502);
#121=CONICAL_SURFACE('',#3465,1.9,0.785398163397448);
#142=SHAPE_REPRESENTATION_RELATIONSHIP('SRR','None',#5560,#152);
#152=ADVANCED_BREP_SHAPE_REPRESENTATION('',(#172),#5496);
#162=STYLED_ITEM('',(#5701),#172);
#172=MANIFOLD_SOLID_BREP('Body1',#3209);
#190=FACE_BOUND('',#630,.T.);
#284=PLANE('',#3468);
#285=PLANE('',#3471);
#286=PLANE('',#3472);
#287=PLANE('',#3477);
#288=PLANE('',#3480);
#434=FACE_OUTER_BOUND('',#621,.T.);
#435=FACE_OUTER_BOUND('',#622,.T.);
#436=FACE_OUTER_BOUND('',#623,.T.);
#437=FACE_OUTER_BOUND('',#624,.T.);
#438=FACE_OUTER_BOUND('',#625,.T.);
#439=FACE_OUTER_BOUND('',#626,.T.);
#440=FACE_OUTER_BOUND('',#627,.T.);
#441=FACE_OUTER_BOUND('',#628,.T.);
#442=FACE_OUTER_BOUND('',#629,.T.);
#621=EDGE_LOOP('',(#2688,#2689,#2690,#2691));
#622=EDGE_LOOP('',(#2692));
#623=EDGE_LOOP('',(#2693,#2694,#2695,#2696));
#624=EDGE_LOOP('',(#2697,#2698,#2699,#2700));
#625=EDGE_LOOP('',(#2701,#2702,#2703,#2704));
#626=EDGE_LOOP('',(#2705,#2706,#2707,#2708));
#627=EDGE_LOOP('',(#2709,#2710,#2711,#2712));
#628=EDGE_LOOP('',(#2713,#2714,#2715,#2716));
#629=EDGE_LOOP('',(#2717));
#630=EDGE_LOOP('',(#2718,#2719,#2720,#2721));
#942=LINE('',#5090,#1273);
#943=LINE('',#5096,#1274);
#944=LINE('',#5100,#1275);
#945=LINE('',#5102,#1276);
#946=LINE('',#5104,#1277);
#947=LINE('',#5105,#1278);
#948=LINE('',#5110,#1279);
#949=LINE('',#5115,#1280);
#950=LINE('',#5119,#1281);
#951=LINE('',#5121,#1282);
#1273=VECTOR('',#4131,1.9);
#1274=VECTOR('',#4140,2.);
#1275=VECTOR('',#4143,1.);
#1276=VECTOR('',#4144,1.);
#1277=VECTOR('',#4145,1.);
#1278=VECTOR('',#4146,1.);
#1279=VECTOR('',#4151,1.);
#1280=VECTOR('',#4158,1.);
#1281=VECTOR('',#4163,1.);
#1282=VECTOR('',#4166,1.);
#1401=CIRCLE('',#3466,1.8);
#1402=CIRCLE('',#3467,2.);
#1403=CIRCLE('',#3470,2.);
#1404=CIRCLE('',#3473,0.5);
#1405=CIRCLE('',#3474,0.5);
#1406=CIRCLE('',#3476,0.5);
#1407=CIRCLE('',#3478,0.5);
#1622=VERTEX_POINT('',#5087);
#1623=VERTEX_POINT('',#5089);
#1624=VERTEX_POINT('',#5094);
#1625=VERTEX_POINT('',#5098);
#1626=VERTEX_POINT('',#5099);
#1627=VERTEX_POINT('',#5101);
#1628=VERTEX_POINT('',#5103);
#1629=VERTEX_POINT('',#5107);
#1630=VERTEX_POINT('',#5109);
#1631=VERTEX_POINT('',#5113);
#1632=VERTEX_POINT('',#5117);
#1994=EDGE_CURVE('',#1622,#1622,#1401,.T.);
#1995=EDGE_CURVE('',#1622,#1623,#942,.T.);
#1996=EDGE_CURVE('',#1623,#1623,#1402,.T.);
#1997=EDGE_CURVE('',#1624,#1624,#1403,.T.);
#1998=EDGE_CURVE('',#1624,#1623,#943,.T.);
#1999=EDGE_CURVE('',#1625,#1626,#944,.T.);
#2000=EDGE_CURVE('',#1627,#1625,#945,.T.);
#2001=EDGE_CURVE('',#1628,#1627,#946,.T.);
#2002=EDGE_CURVE('',#1626,#1628,#947,.T.);
#2003=EDGE_CURVE('',#1627,#1629,#1404,.T.);
#2004=EDGE_CURVE('',#1630,#1629,#948,.T.);
#2005=EDGE_CURVE('',#1630,#1628,#1405,.T.);
#2006=EDGE_CURVE('',#1625,#1631,#1406,.T.);
#2007=EDGE_CURVE('',#1629,#1631,#949,.T.);
#2008=EDGE_CURVE('',#1632,#1626,#1407,.T.);
#2009=EDGE_CURVE('',#1631,#1632,#950,.T.);
#2010=EDGE_CURVE('',#1632,#1630,#951,.T.);
#2688=ORIENTED_EDGE('',*,*,#1994,.T.);
#2689=ORIENTED_EDGE('',*,*,#1995,.T.);
#2690=ORIENTED_EDGE('',*,*,#1996,.T.);
#2691=ORIENTED_EDGE('',*,*,#1995,.F.);
#2692=ORIENTED_EDGE('',*,*,#1994,.F.);
#2693=ORIENTED_EDGE('',*,*,#1997,.F.);
#2694=ORIENTED_EDGE('',*,*,#1998,.T.);
#2695=ORIENTED_EDGE('',*,*,#1996,.F.);
#2696=ORIENTED_EDGE('',*,*,#1998,.F.);
#2697=ORIENTED_EDGE('',*,*,#1999,.F.);
#2698=ORIENTED_EDGE('',*,*,#2000,.F.);
#2699=ORIENTED_EDGE('',*,*,#2001,.F.);
#2700=ORIENTED_EDGE('',*,*,#2002,.F.);
#2701=ORIENTED_EDGE('',*,*,#2001,.T.);
#2702=ORIENTED_EDGE('',*,*,#2003,.T.);
#2703=ORIENTED_EDGE('',*,*,#2004,.F.);
#2704=ORIENTED_EDGE('',*,*,#2005,.T.);
#2705=ORIENTED_EDGE('',*,*,#2000,.T.);
#2706=ORIENTED_EDGE('',*,*,#2006,.T.);
#2707=ORIENTED_EDGE('',*,*,#2007,.F.);
#2708=ORIENTED_EDGE('',*,*,#2003,.F.);
#2709=ORIENTED_EDGE('',*,*,#1999,.T.);
#2710=ORIENTED_EDGE('',*,*,#2008,.F.);
#2711=ORIENTED_EDGE('',*,*,#2009,.F.);
#2712=ORIENTED_EDGE('',*,*,#2006,.F.);
#2713=ORIENTED_EDGE('',*,*,#2002,.T.);
#2714=ORIENTED_EDGE('',*,*,#2005,.F.);
#2715=ORIENTED_EDGE('',*,*,#2010,.F.);
#2716=ORIENTED_EDGE('',*,*,#2008,.T.);
#2717=ORIENTED_EDGE('',*,*,#1997,.T.);
#2718=ORIENTED_EDGE('',*,*,#2007,.T.);
#2719=ORIENTED_EDGE('',*,*,#2009,.T.);
#2720=ORIENTED_EDGE('',*,*,#2010,.T.);
#2721=ORIENTED_EDGE('',*,*,#2004,.T.);
#3016=CYLINDRICAL_SURFACE('',#3469,2.);
#3017=CYLINDRICAL_SURFACE('',#3475,0.5);
#3018=CYLINDRICAL_SURFACE('',#3479,0.5);
#3128=ADVANCED_FACE('',(#434),#121,.T.);
#3129=ADVANCED_FACE('',(#435),#284,.T.);
#3130=ADVANCED_FACE('',(#436),#3016,.T.);
#3131=ADVANCED_FACE('',(#437),#285,.F.);
#3132=ADVANCED_FACE('',(#438),#286,.T.);
#3133=ADVANCED_FACE('',(#439),#3017,.F.);
#3134=ADVANCED_FACE('',(#440),#287,.F.);
#3135=ADVANCED_FACE('',(#441),#3018,.F.);
#3136=ADVANCED_FACE('',(#442,#190),#288,.T.);
#3209=CLOSED_SHELL('',(#3128,#3129,#3130,#3131,#3132,#3133,#3134,#3135,
#3136));
#3464=AXIS2_PLACEMENT_3D('',#5085,#4125,#4126);
#3465=AXIS2_PLACEMENT_3D('',#5086,#4127,#4128);
#3466=AXIS2_PLACEMENT_3D('',#5088,#4129,#4130);
#3467=AXIS2_PLACEMENT_3D('',#5091,#4132,#4133);
#3468=AXIS2_PLACEMENT_3D('',#5092,#4134,#4135);
#3469=AXIS2_PLACEMENT_3D('',#5093,#4136,#4137);
#3470=AXIS2_PLACEMENT_3D('',#5095,#4138,#4139);
#3471=AXIS2_PLACEMENT_3D('',#5097,#4141,#4142);
#3472=AXIS2_PLACEMENT_3D('',#5106,#4147,#4148);
#3473=AXIS2_PLACEMENT_3D('',#5108,#4149,#4150);
#3474=AXIS2_PLACEMENT_3D('',#5111,#4152,#4153);
#3475=AXIS2_PLACEMENT_3D('',#5112,#4154,#4155);
#3476=AXIS2_PLACEMENT_3D('',#5114,#4156,#4157);
#3477=AXIS2_PLACEMENT_3D('',#5116,#4159,#4160);
#3478=AXIS2_PLACEMENT_3D('',#5118,#4161,#4162);
#3479=AXIS2_PLACEMENT_3D('',#5120,#4164,#4165);
#3480=AXIS2_PLACEMENT_3D('',#5122,#4167,#4168);
#4125=DIRECTION('axis',(0.,0.,1.));
#4126=DIRECTION('refdir',(1.,0.,0.));
#4127=DIRECTION('center_axis',(0.,0.,1.));
#4128=DIRECTION('ref_axis',(1.,0.,0.));
#4129=DIRECTION('center_axis',(0.,0.,1.));
#4130=DIRECTION('ref_axis',(1.,0.,0.));
#4131=DIRECTION('',(-0.707106781186547,8.65956056235493E-17,0.707106781186548));
#4132=DIRECTION('center_axis',(0.,0.,-1.));
#4133=DIRECTION('ref_axis',(1.,0.,0.));
#4134=DIRECTION('center_axis',(0.,0.,-1.));
#4135=DIRECTION('ref_axis',(-1.,0.,0.));
#4136=DIRECTION('center_axis',(0.,0.,1.));
#4137=DIRECTION('ref_axis',(1.,0.,0.));
#4138=DIRECTION('center_axis',(0.,0.,1.));
#4139=DIRECTION('ref_axis',(1.,0.,0.));
#4140=DIRECTION('',(0.,0.,-1.));
#4141=DIRECTION('center_axis',(0.,0.,-1.));
#4142=DIRECTION('ref_axis',(1.,0.,0.));
#4143=DIRECTION('',(1.,0.,0.));
#4144=DIRECTION('',(0.,1.,0.));
#4145=DIRECTION('',(-1.,0.,0.));
#4146=DIRECTION('',(0.,-1.,0.));
#4147=DIRECTION('center_axis',(0.,1.,0.));
#4148=DIRECTION('ref_axis',(1.,0.,0.));
#4149=DIRECTION('center_axis',(0.,1.,0.));
#4150=DIRECTION('ref_axis',(1.,0.,0.));
#4151=DIRECTION('',(-1.,0.,0.));
#4152=DIRECTION('center_axis',(0.,1.,0.));
#4153=DIRECTION('ref_axis',(1.,0.,0.));
#4154=DIRECTION('center_axis',(0.,1.,0.));
#4155=DIRECTION('ref_axis',(1.,0.,0.));
#4156=DIRECTION('center_axis',(0.,1.,0.));
#4157=DIRECTION('ref_axis',(1.,0.,0.));
#4158=DIRECTION('',(0.,1.,0.));
#4159=DIRECTION('center_axis',(0.,1.,0.));
#4160=DIRECTION('ref_axis',(1.,0.,0.));
#4161=DIRECTION('center_axis',(0.,1.,0.));
#4162=DIRECTION('ref_axis',(1.,0.,0.));
#4163=DIRECTION('',(1.,0.,0.));
#4164=DIRECTION('center_axis',(0.,1.,0.));
#4165=DIRECTION('ref_axis',(1.,0.,0.));
#4166=DIRECTION('',(0.,-1.,0.));
#4167=DIRECTION('center_axis',(0.,0.,1.));
#4168=DIRECTION('ref_axis',(1.,0.,0.));
#5085=CARTESIAN_POINT('',(0.,0.,0.));
#5086=CARTESIAN_POINT('Origin',(0.,0.,0.1));
#5087=CARTESIAN_POINT('',(-1.8,-2.20436423846524E-16,0.));
#5088=CARTESIAN_POINT('Origin',(0.,0.,0.));
#5089=CARTESIAN_POINT('',(-2.,2.44929359829471E-16,0.2));
#5090=CARTESIAN_POINT('',(-1.9,2.32682891837997E-16,0.1));
#5091=CARTESIAN_POINT('Origin',(0.,0.,0.2));
#5092=CARTESIAN_POINT('Origin',(1.9,0.,0.));
#5093=CARTESIAN_POINT('Origin',(0.,0.,0.25));
#5094=CARTESIAN_POINT('',(-2.,-2.44929359829471E-16,0.4));
#5095=CARTESIAN_POINT('Origin',(0.,0.,0.4));
#5096=CARTESIAN_POINT('',(-2.,-2.44929359829471E-16,0.25));
#5097=CARTESIAN_POINT('Origin',(0.,0.,0.3));
#5098=CARTESIAN_POINT('',(-0.4,0.6,0.3));
#5099=CARTESIAN_POINT('',(0.4,0.6,0.3));
#5100=CARTESIAN_POINT('',(0.,0.6,0.3));
#5101=CARTESIAN_POINT('',(-0.4,0.2,0.3));
#5102=CARTESIAN_POINT('',(-0.4,0.2,0.3));
#5103=CARTESIAN_POINT('',(0.4,0.2,0.3));
#5104=CARTESIAN_POINT('',(0.,0.2,0.3));
#5105=CARTESIAN_POINT('',(0.4,0.2,0.3));
#5106=CARTESIAN_POINT('Origin',(0.,0.2,0.));
#5107=CARTESIAN_POINT('',(-0.3,0.2,0.4));
#5108=CARTESIAN_POINT('Origin',(0.,0.2,0.));
#5109=CARTESIAN_POINT('',(0.3,0.2,0.4));
#5110=CARTESIAN_POINT('',(0.,0.2,0.4));
#5111=CARTESIAN_POINT('Origin',(0.,0.2,0.));
#5112=CARTESIAN_POINT('Origin',(0.,0.2,0.));
#5113=CARTESIAN_POINT('',(-0.3,0.6,0.4));
#5114=CARTESIAN_POINT('Origin',(0.,0.6,0.));
#5115=CARTESIAN_POINT('',(-0.3,0.2,0.4));
#5116=CARTESIAN_POINT('Origin',(0.,0.6,0.));
#5117=CARTESIAN_POINT('',(0.3,0.6,0.4));
#5118=CARTESIAN_POINT('Origin',(0.,0.6,0.));
#5119=CARTESIAN_POINT('',(0.,0.6,0.4));
#5120=CARTESIAN_POINT('Origin',(0.,0.2,0.));
#5121=CARTESIAN_POINT('',(0.3,0.2,0.4));
#5122=CARTESIAN_POINT('Origin',(0.,0.,0.4));
#5483=UNCERTAINTY_MEASURE_WITH_UNIT(LENGTH_MEASURE(0.001),#5503,
'DISTANCE_ACCURACY_VALUE',
'Maximum model space distance between geometric entities at asserted c
onnectivities');
#5489=UNCERTAINTY_MEASURE_WITH_UNIT(LENGTH_MEASURE(0.001),#5503,
'DISTANCE_ACCURACY_VALUE',
'Maximum model space distance between geometric entities at asserted c
onnectivities');
#5496=(
GEOMETRIC_REPRESENTATION_CONTEXT(3)
GLOBAL_UNCERTAINTY_ASSIGNED_CONTEXT((#5483))
GLOBAL_UNIT_ASSIGNED_CONTEXT((#5503,#5505,#5506))
REPRESENTATION_CONTEXT('','3D')
);
#5502=(
GEOMETRIC_REPRESENTATION_CONTEXT(3)
GLOBAL_UNCERTAINTY_ASSIGNED_CONTEXT((#5489))
GLOBAL_UNIT_ASSIGNED_CONTEXT((#5503,#5505,#5506))
REPRESENTATION_CONTEXT('','3D')
);
#5503=(
LENGTH_UNIT()
NAMED_UNIT(*)
SI_UNIT(.CENTI.,.METRE.)
);
#5505=(
NAMED_UNIT(*)
PLANE_ANGLE_UNIT()
SI_UNIT($,.RADIAN.)
);
#5506=(
NAMED_UNIT(*)
SI_UNIT($,.STERADIAN.)
SOLID_ANGLE_UNIT()
);
#5513=SHAPE_DEFINITION_REPRESENTATION(#5525,#5560);
#5525=PRODUCT_DEFINITION_SHAPE('',$,#5573);
#5560=SHAPE_REPRESENTATION('',(#3464),#5496);
#5566=PRODUCT_DEFINITION_CONTEXT('part definition',#5604,'design');
#5573=PRODUCT_DEFINITION('Rubber base','Rubber base',#5585,
#5566);
#5585=PRODUCT_DEFINITION_FORMATION('',$,#5612);
#5604=APPLICATION_CONTEXT(
'Core Data for Automotive Mechanical Design Process');
#5605=PRODUCT_CONTEXT('part definition',#5604,'mechanical');
#5612=PRODUCT('Rubber base','Rubber base','Rubber base',(#5605));
#5695=COLOUR_RGB('Black',0.12,0.14,0.17);
#5696=FILL_AREA_STYLE_COLOUR('',#5695);
#5697=FILL_AREA_STYLE('',(#5696));
#5698=SURFACE_STYLE_FILL_AREA(#5697);
#5699=SURFACE_SIDE_STYLE('',(#5698));
#5700=SURFACE_STYLE_USAGE(.BOTH.,#5699);
#5701=PRESENTATION_STYLE_ASSIGNMENT((#5700));
ENDSEC;
END-ISO-10303-21;
